ISO-10303-21;
HEADER;
/* Generated by software containing ST-Developer
 * from STEP Tools, Inc. (www.steptools.com) 
 */

FILE_DESCRIPTION(
/* description */ ('Cam-and-follower valve demonstrator'),
/* implementation_level */ '2;1');

FILE_NAME(
/* name */ 'Axial keeper (1).step',
/* time_stamp */ '2026-10-28T03:25:17-07:00',
/* author */ (''),
/* organization */ (''),
/* preprocessor_version */ 'ST-DEVELOPER v20.2',
/* originating_system */ 'Autodesk Translation Framework v15.17.0.0',
/* authorisation */ '');

FILE_SCHEMA (('AUTOMOTIVE_DESIGN { 1 0 10303 214 3 1 1 }'));
ENDSEC;

DATA;
#10=MECHANICAL_DESIGN_GEOMETRIC_PRESENTATION_REPRESENTATION('',(#449),#12896);
#370=SHAPE_REPRESENTATION_RELATIONSHIP('SRR','None',#13089,#406);
#406=ADVANCED_BREP_SHAPE_REPRESENTATION('',(#490),#12889);
#449=STYLED_ITEM('',(#13316),#490);
#490=MANIFOLD_SOLID_BREP('Body1',#6218);
#650=FACE_BOUND('',#1940,.T.);
#651=FACE_BOUND('',#1942,.T.);
#949=CIRCLE('',#7274,0.225);
#950=CIRCLE('',#7275,0.225);
#951=CIRCLE('',#7277,1.);
#952=CIRCLE('',#7278,1.);
#1085=CYLINDRICAL_SURFACE('',#7273,0.225);
#1086=CYLINDRICAL_SURFACE('',#7276,1.);
#1414=FACE_OUTER_BOUND('',#1937,.T.);
#1415=FACE_OUTER_BOUND('',#1938,.T.);
#1416=FACE_OUTER_BOUND('',#1939,.T.);
#1417=FACE_OUTER_BOUND('',#1941,.T.);
#1937=EDGE_LOOP('',(#5413,#5414,#5415,#5416));
#1938=EDGE_LOOP('',(#5417,#5418,#5419,#5420));
#1939=EDGE_LOOP('',(#5421));
#1940=EDGE_LOOP('',(#5422));
#1941=EDGE_LOOP('',(#5423));
#1942=EDGE_LOOP('',(#5424));
#2349=LINE('',#12546,#2771);
#2350=LINE('',#12552,#2772);
#2771=VECTOR('',#9074,0.225);
#2772=VECTOR('',#9081,1.);
#3284=VERTEX_POINT('',#12543);
#3285=VERTEX_POINT('',#12545);
#3286=VERTEX_POINT('',#12549);
#3287=VERTEX_POINT('',#12551);
#4003=EDGE_CURVE('',#3284,#3284,#949,.T.);
#4004=EDGE_CURVE('',#3284,#3285,#2349,.T.);
#4005=EDGE_CURVE('',#3285,#3285,#950,.T.);
#4006=EDGE_CURVE('',#3286,#3286,#951,.T.);
#4007=EDGE_CURVE('',#3286,#3287,#2350,.T.);
#4008=EDGE_CURVE('',#3287,#3287,#952,.T.);
#5413=ORIENTED_EDGE('',*,*,#4003,.F.);
#5414=ORIENTED_EDGE('',*,*,#4004,.T.);
#5415=ORIENTED_EDGE('',*,*,#4005,.T.);
#5416=ORIENTED_EDGE('',*,*,#4004,.F.);
#5417=ORIENTED_EDGE('',*,*,#4006,.F.);
#5418=ORIENTED_EDGE('',*,*,#4007,.T.);
#5419=ORIENTED_EDGE('',*,*,#4008,.T.);
#5420=ORIENTED_EDGE('',*,*,#4007,.F.);
#5421=ORIENTED_EDGE('',*,*,#4006,.T.);
#5422=ORIENTED_EDGE('',*,*,#4003,.T.);
#5423=ORIENTED_EDGE('',*,*,#4008,.F.);
#5424=ORIENTED_EDGE('',*,*,#4005,.F.);
#5776=PLANE('',#7279);
#5777=PLANE('',#7280);
#6130=ADVANCED_FACE('',(#1414),#1085,.F.);
#6131=ADVANCED_FACE('',(#1415),#1086,.T.);
#6132=ADVANCED_FACE('',(#1416,#650),#5776,.T.);
#6133=ADVANCED_FACE('',(#1417,#651),#5777,.F.);
#6218=CLOSED_SHELL('',(#6130,#6131,#6132,#6133));
#7272=AXIS2_PLACEMENT_3D('',#12541,#9068,#9069);
#7273=AXIS2_PLACEMENT_3D('',#12542,#9070,#9071);
#7274=AXIS2_PLACEMENT_3D('',#12544,#9072,#9073);
#7275=AXIS2_PLACEMENT_3D('',#12547,#9075,#9076);
#7276=AXIS2_PLACEMENT_3D('',#12548,#9077,#9078);
#7277=AXIS2_PLACEMENT_3D('',#12550,#9079,#9080);
#7278=AXIS2_PLACEMENT_3D('',#12553,#9082,#9083);
#7279=AXIS2_PLACEMENT_3D('',#12554,#9084,#9085);
#7280=AXIS2_PLACEMENT_3D('',#12555,#9086,#9087);
#9068=DIRECTION('axis',(0.,0.,1.));
#9069=DIRECTION('refdir',(1.,0.,0.));
#9070=DIRECTION('center_axis',(0.,1.,0.));
#9071=DIRECTION('ref_axis',(1.,0.,0.));
#9072=DIRECTION('center_axis',(0.,-1.,0.));
#9073=DIRECTION('ref_axis',(1.,0.,0.));
#9074=DIRECTION('',(0.,-1.,0.));
#9075=DIRECTION('center_axis',(0.,-1.,0.));
#9076=DIRECTION('ref_axis',(1.,0.,0.));
#9077=DIRECTION('center_axis',(0.,1.,0.));
#9078=DIRECTION('ref_axis',(1.,0.,0.));
#9079=DIRECTION('center_axis',(0.,1.,0.));
#9080=DIRECTION('ref_axis',(1.,0.,0.));
#9081=DIRECTION('',(0.,-1.,0.));
#9082=DIRECTION('center_axis',(0.,1.,0.));
#9083=DIRECTION('ref_axis',(1.,0.,0.));
#9084=DIRECTION('center_axis',(0.,1.,0.));
#9085=DIRECTION('ref_axis',(1.,0.,0.));
#9086=DIRECTION('center_axis',(0.,1.,0.));
#9087=DIRECTION('ref_axis',(1.,0.,0.));
#12541=CARTESIAN_POINT('',(0.,0.,0.));
#12542=CARTESIAN_POINT('Origin',(0.,6.5,4.));
#12543=CARTESIAN_POINT('',(-0.225,6.7,4.));
#12544=CARTESIAN_POINT('Origin',(0.,6.7,4.));
#12545=CARTESIAN_POINT('',(-0.225,6.5,4.));
#12546=CARTESIAN_POINT('',(-0.225,6.5,4.));
#12547=CARTESIAN_POINT('Origin',(0.,6.5,4.));
#12548=CARTESIAN_POINT('Origin',(0.,6.5,4.));
#12549=CARTESIAN_POINT('',(-1.,6.7,4.));
#12550=CARTESIAN_POINT('Origin',(0.,6.7,4.));
#12551=CARTESIAN_POINT('',(-1.,6.5,4.));
#12552=CARTESIAN_POINT('',(-1.,6.5,4.));
#12553=CARTESIAN_POINT('Origin',(0.,6.5,4.));
#12554=CARTESIAN_POINT('Origin',(0.,6.7,4.));
#12555=CARTESIAN_POINT('Origin',(0.,6.5,4.));
#12846=UNCERTAINTY_MEASURE_WITH_UNIT(LENGTH_MEASURE(0.001),#12897,
'DISTANCE_ACCURACY_VALUE',
'Maximum model space distance between geometric entities at asserted c
onnectivities');
#12853=UNCERTAINTY_MEASURE_WITH_UNIT(LENGTH_MEASURE(0.001),#12897,
'DISTANCE_ACCURACY_VALUE',
'Maximum model space distance between geometric entities at asserted c
onnectivities');
#12889=(
GEOMETRIC_REPRESENTATION_CONTEXT(3)
GLOBAL_UNCERTAINTY_ASSIGNED_CONTEXT((#12846))
GLOBAL_UNIT_ASSIGNED_CONTEXT((#12897,#12899,#12900))
REPRESENTATION_CONTEXT('','3D')
);
#12896=(
GEOMETRIC_REPRESENTATION_CONTEXT(3)
GLOBAL_UNCERTAINTY_ASSIGNED_CONTEXT((#12853))
GLOBAL_UNIT_ASSIGNED_CONTEXT((#12897,#12899,#12900))
REPRESENTATION_CONTEXT('','3D')
);
#12897=(
LENGTH_UNIT()
NAMED_UNIT(*)
SI_UNIT(.CENTI.,.METRE.)
);
#12899=(
NAMED_UNIT(*)
PLANE_ANGLE_UNIT()
SI_UNIT($,.RADIAN.)
);
#12900=(
NAMED_UNIT(*)
SI_UNIT($,.STERADIAN.)
SOLID_ANGLE_UNIT()
);
#12936=SHAPE_DEFINITION_REPRESENTATION(#12985,#13089);
#12985=PRODUCT_DEFINITION_SHAPE('',$,#13132);
#13089=SHAPE_REPRESENTATION('',(#7272),#12889);
#13096=PRODUCT_DEFINITION_CONTEXT('part definition',#13224,'design');
#13132=PRODUCT_DEFINITION('Axial keeper (1)','Axial keeper (1)',#13174,#13096);
#13174=PRODUCT_DEFINITION_FORMATION('',$,#13261);
#13224=APPLICATION_CONTEXT(
'Core Data for Automotive Mechanical Design Process');
#13225=PRODUCT_CONTEXT('part definition',#13224,'mechanical');
#13261=PRODUCT('Axial keeper (1)','Axial keeper (1)','Axial keeper (1)',(#13225));
#13310=COLOUR_RGB('Light Blue',0.38,0.62,0.78);
#13311=FILL_AREA_STYLE_COLOUR('',#13310);
#13312=FILL_AREA_STYLE('',(#13311));
#13313=SURFACE_STYLE_FILL_AREA(#13312);
#13314=SURFACE_SIDE_STYLE('',(#13313));
#13315=SURFACE_STYLE_USAGE(.BOTH.,#13314);
#13316=PRESENTATION_STYLE_ASSIGNMENT((#13315));
ENDSEC;
END-ISO-10303-21;
